ISO-10303-21;
HEADER;
/* Generated by software containing ST-Developer
 * from STEP Tools, Inc. (www.steptools.com) 
 */

FILE_DESCRIPTION(
/* description */ (''),
/* implementation_level */ '2;1');

FILE_NAME(
/* name */ 'Spring_01.step',
/* time_stamp */ '2026-10-23T17:00:58+06:00',
/* author */ (''),
/* organization */ (''),
/* preprocessor_version */ 'ST-DEVELOPER v20.2',
/* originating_system */ 'Autodesk Translation Framework v15.15.0.0',
/* authorisation */ '');

FILE_SCHEMA (('AUTOMOTIVE_DESIGN { 1 0 10303 214 3 1 1 }'));
ENDSEC;

DATA;
#10=MECHANICAL_DESIGN_GEOMETRIC_PRESENTATION_REPRESENTATION('',(#108),#11385);
#69=B_SPLINE_SURFACE_WITH_KNOTS('',3,3,((#8625,#8626,#8627,#8628,#8629,
#8630,#8631,#8632,#8633,#8634,#8635,#8636,#8637,#8638,#8639,#8640,#8641,
#8642,#8643,#8644,#8645,#8646,#8647,#8648,#8649,#8650,#8651,#8652,#8653,
#8654,#8655,#8656,#8657,#8658,#8659,#8660,#8661),(#8662,#8663,#8664,#8665,
#8666,#8667,#8668,#8669,#8670,#8671,#8672,#8673,#8674,#8675,#8676,#8677,
#8678,#8679,#8680,#8681,#8682,#8683,#8684,#8685,#8686,#8687,#8688,#8689,
#8690,#8691,#8692,#8693,#8694,#8695,#8696,#8697,#8698),(#8699,#8700,#8701,
#8702,#8703,#8704,#8705,#8706,#8707,#8708,#8709,#8710,#8711,#8712,#8713,
#8714,#8715,#8716,#8717,#8718,#8719,#8720,#8721,#8722,#8723,#8724,#8725,
#8726,#8727,#8728,#8729,#8730,#8731,#8732,#8733,#8734,#8735),(#8736,#8737,
#8738,#8739,#8740,#8741,#8742,#8743,#8744,#8745,#8746,#8747,#8748,#8749,
#8750,#8751,#8752,#8753,#8754,#8755,#8756,#8757,#8758,#8759,#8760,#8761,
#8762,#8763,#8764,#8765,#8766,#8767,#8768,#8769,#8770,#8771,#8772),(#8773,
#8774,#8775,#8776,#8777,#8778,#8779,#8780,#8781,#8782,#8783,#8784,#8785,
#8786,#8787,#8788,#8789,#8790,#8791,#8792,#8793,#8794,#8795,#8796,#8797,
#8798,#8799,#8800,#8801,#8802,#8803,#8804,#8805,#8806,#8807,#8808,#8809),
(#8810,#8811,#8812,#8813,#8814,#8815,#8816,#8817,#8818,#8819,#8820,#8821,
#8822,#8823,#8824,#8825,#8826,#8827,#8828,#8829,#8830,#8831,#8832,#8833,
#8834,#8835,#8836,#8837,#8838,#8839,#8840,#8841,#8842,#8843,#8844,#8845,
#8846),(#8847,#8848,#8849,#8850,#8851,#8852,#8853,#8854,#8855,#8856,#8857,
#8858,#8859,#8860,#8861,#8862,#8863,#8864,#8865,#8866,#8867,#8868,#8869,
#8870,#8871,#8872,#8873,#8874,#8875,#8876,#8877,#8878,#8879,#8880,#8881,
#8882,#8883),(#8884,#8885,#8886,#8887,#8888,#8889,#8890,#8891,#8892,#8893,
#8894,#8895,#8896,#8897,#8898,#8899,#8900,#8901,#8902,#8903,#8904,#8905,
#8906,#8907,#8908,#8909,#8910,#8911,#8912,#8913,#8914,#8915,#8916,#8917,
#8918,#8919,#8920),(#8921,#8922,#8923,#8924,#8925,#8926,#8927,#8928,#8929,
#8930,#8931,#8932,#8933,#8934,#8935,#8936,#8937,#8938,#8939,#8940,#8941,
#8942,#8943,#8944,#8945,#8946,#8947,#8948,#8949,#8950,#8951,#8952,#8953,
#8954,#8955,#8956,#8957),(#8958,#8959,#8960,#8961,#8962,#8963,#8964,#8965,
#8966,#8967,#8968,#8969,#8970,#8971,#8972,#8973,#8974,#8975,#8976,#8977,
#8978,#8979,#8980,#8981,#8982,#8983,#8984,#8985,#8986,#8987,#8988,#8989,
#8990,#8991,#8992,#8993,#8994),(#8995,#8996,#8997,#8998,#8999,#9000,#9001,
#9002,#9003,#9004,#9005,#9006,#9007,#9008,#9009,#9010,#9011,#9012,#9013,
#9014,#9015,#9016,#9017,#9018,#9019,#9020,#9021,#9022,#9023,#9024,#9025,
#9026,#9027,#9028,#9029,#9030,#9031),(#9032,#9033,#9034,#9035,#9036,#9037,
#9038,#9039,#9040,#9041,#9042,#9043,#9044,#9045,#9046,#9047,#9048,#9049,
#9050,#9051,#9052,#9053,#9054,#9055,#9056,#9057,#9058,#9059,#9060,#9061,
#9062,#9063,#9064,#9065,#9066,#9067,#9068)),.UNSPECIFIED.,.T.,.F.,.F.,(4,
1,1,1,1,1,1,1,1,4),(4,1,1,1,1,1,1,1,1,1,1,1,1,1,1,1,1,1,1,1,1,1,1,1,1,1,
1,1,1,1,1,1,1,1,4),(-3.14159265358979,-2.46839422782055,-2.24399475256414,
-1.79519580205131,-1.12199737628207,-0.448798950512828,0.448798950512828,
1.34639685153848,2.24399475256414,3.14159265358979),(0.,0.490873852123405,
0.98174770424681,1.96349540849362,2.94524311274043,3.92699081698724,4.90873852123405,
5.89048622548086,6.87223392972767,7.85398163397448,8.83572933822129,9.8174770424681,
10.7992247467149,11.7809724509617,12.7627201552085,13.7444678594553,14.7262155637022,
15.707963267949,16.6897109721958,17.6714586764426,18.6532063806894,19.6349540849362,
20.616701789183,21.5984494934298,22.5801971976766,23.5619449019234,24.5436926061703,
25.5254403104171,26.5071880146639,27.4889357189107,28.4706834231575,29.4524311274043,
30.4341788316511,30.9250526837745,31.4159265358979),.UNSPECIFIED.);
#73=TOROIDAL_SURFACE('',#5790,1.,0.25);
#82=SHAPE_REPRESENTATION_RELATIONSHIP('SRR','None',#11434,#95);
#95=ADVANCED_BREP_SHAPE_REPRESENTATION('',(#121),#11374);
#108=STYLED_ITEM('',(#11567),#121);
#121=MANIFOLD_SOLID_BREP('Spring_01',#5344);
#150=FACE_BOUND('',#1107,.T.);
#175=B_SPLINE_CURVE_WITH_KNOTS('',3,(#8581,#8582,#8583,#8584,#8585,#8586,
#8587,#8588,#8589,#8590,#8591,#8592,#8593,#8594,#8595,#8596,#8597,#8598,
#8599,#8600,#8601,#8602,#8603,#8604,#8605,#8606,#8607,#8608,#8609,#8610,
#8611,#8612,#8613,#8614,#8615,#8616,#8617,#8618,#8619,#8620,#8621,#8622,
#8623,#8624),.UNSPECIFIED.,.F.,.F.,(4,2,2,2,2,2,2,2,2,2,2,2,2,2,2,2,2,2,
2,2,2,4),(-0.181685657499379,-0.180553745361431,-0.170622434730818,-0.170447684206912,
-0.167737370927117,-0.166612489538818,-0.16575101153334,-0.16478662015514,
-0.16342132279605,-0.160072321773434,-0.151029759575816,-0.145020173168477,
-0.126301129887337,-0.111561605759352,-0.101015311157688,-0.0928919097586381,
-0.0856896815461206,-0.0776947291824182,-0.0660486167614411,-0.0443043011100664,
0.,0.000811103137473634),.UNSPECIFIED.);
#176=B_SPLINE_CURVE_WITH_KNOTS('',3,(#9070,#9071,#9072,#9073,#9074,#9075,
#9076,#9077,#9078,#9079,#9080,#9081,#9082,#9083,#9084,#9085,#9086,#9087,
#9088,#9089,#9090,#9091,#9092,#9093,#9094,#9095,#9096,#9097,#9098,#9099,
#9100,#9101,#9102,#9103,#9104,#9105,#9106),.UNSPECIFIED.,.F.,.F.,(4,1,1,
1,1,1,1,1,1,1,1,1,1,1,1,1,1,1,1,1,1,1,1,1,1,1,1,1,1,1,1,1,1,1,4),(0.,0.490873852123405,
0.98174770424681,1.96349540849362,2.94524311274043,3.92699081698724,4.90873852123405,
5.89048622548086,6.87223392972767,7.85398163397448,8.83572933822129,9.8174770424681,
10.7992247467149,11.7809724509617,12.7627201552085,13.7444678594553,14.7262155637022,
15.707963267949,16.6897109721958,17.6714586764426,18.6532063806894,19.6349540849362,
20.616701789183,21.5984494934298,22.5801971976766,23.5619449019234,24.5436926061703,
25.5254403104171,26.5071880146639,27.4889357189107,28.4706834231575,29.4524311274043,
30.4341788316511,30.9250526837745,31.4159265358979),.UNSPECIFIED.);
#402=CIRCLE('',#5791,0.25);
#403=CIRCLE('',#5792,0.75);
#404=CIRCLE('',#5793,0.25);
#405=CIRCLE('',#5794,0.25);
#762=FACE_OUTER_BOUND('',#1106,.T.);
#763=FACE_OUTER_BOUND('',#1108,.T.);
#764=FACE_OUTER_BOUND('',#1109,.T.);
#1106=EDGE_LOOP('',(#4148,#4149,#4150,#4151));
#1107=EDGE_LOOP('',(#4152,#4153));
#1108=EDGE_LOOP('',(#4154,#4155,#4156,#4157,#4158));
#1109=EDGE_LOOP('',(#4159));
#2446=VERTEX_POINT('',#8575);
#2447=VERTEX_POINT('',#8578);
#2448=VERTEX_POINT('',#8579);
#2449=VERTEX_POINT('',#9069);
#3039=EDGE_CURVE('',#2446,#2446,#402,.T.);
#3040=EDGE_CURVE('',#2446,#2446,#403,.T.);
#3041=EDGE_CURVE('',#2447,#2448,#404,.T.);
#3042=EDGE_CURVE('',#2447,#2448,#175,.T.);
#3043=EDGE_CURVE('',#2448,#2449,#176,.T.);
#3044=EDGE_CURVE('',#2449,#2449,#405,.T.);
#4148=ORIENTED_EDGE('',*,*,#3039,.F.);
#4149=ORIENTED_EDGE('',*,*,#3040,.T.);
#4150=ORIENTED_EDGE('',*,*,#3039,.T.);
#4151=ORIENTED_EDGE('',*,*,#3040,.F.);
#4152=ORIENTED_EDGE('',*,*,#3041,.T.);
#4153=ORIENTED_EDGE('',*,*,#3042,.F.);
#4154=ORIENTED_EDGE('',*,*,#3042,.T.);
#4155=ORIENTED_EDGE('',*,*,#3043,.T.);
#4156=ORIENTED_EDGE('',*,*,#3044,.F.);
#4157=ORIENTED_EDGE('',*,*,#3043,.F.);
#4158=ORIENTED_EDGE('',*,*,#3041,.F.);
#4159=ORIENTED_EDGE('',*,*,#3044,.T.);
#4938=PLANE('',#5795);
#5174=ADVANCED_FACE('',(#762,#150),#73,.T.);
#5175=ADVANCED_FACE('',(#763),#69,.T.);
#5176=ADVANCED_FACE('',(#764),#4938,.T.);
#5344=CLOSED_SHELL('',(#5174,#5175,#5176));
#5789=AXIS2_PLACEMENT_3D('',#8573,#6934,#6935);
#5790=AXIS2_PLACEMENT_3D('',#8574,#6936,#6937);
#5791=AXIS2_PLACEMENT_3D('',#8576,#6938,#6939);
#5792=AXIS2_PLACEMENT_3D('',#8577,#6940,#6941);
#5793=AXIS2_PLACEMENT_3D('',#8580,#6942,#6943);
#5794=AXIS2_PLACEMENT_3D('',#9107,#6944,#6945);
#5795=AXIS2_PLACEMENT_3D('',#9108,#6946,#6947);
#6934=DIRECTION('axis',(0.,0.,1.));
#6935=DIRECTION('refdir',(1.,0.,0.));
#6936=DIRECTION('center_axis',(-1.,0.,0.));
#6937=DIRECTION('ref_axis',(0.,0.,-1.));
#6938=DIRECTION('center_axis',(0.,1.,0.));
#6939=DIRECTION('ref_axis',(0.,0.,1.));
#6940=DIRECTION('center_axis',(1.,0.,0.));
#6941=DIRECTION('ref_axis',(0.,0.,-1.));
#6942=DIRECTION('center_axis',(0.,1.,1.22464679914735E-16));
#6943=DIRECTION('ref_axis',(1.,0.,0.));
#6944=DIRECTION('center_axis',(1.22464679914735E-15,-1.,-1.22464679914735E-16));
#6945=DIRECTION('ref_axis',(1.,1.22464679914735E-15,1.49975978266186E-31));
#6946=DIRECTION('center_axis',(1.22464679914735E-15,-1.,-1.22464679914735E-16));
#6947=DIRECTION('ref_axis',(0.,1.22464679914735E-16,-1.));
#8573=CARTESIAN_POINT('',(0.,0.,0.));
#8574=CARTESIAN_POINT('Origin',(-3.64952178519528,11.2640879581285,17.6));
#8575=CARTESIAN_POINT('',(-3.64952178519528,11.2640879581285,18.35));
#8576=CARTESIAN_POINT('Origin',(-3.64952178519528,11.2640879581285,18.6));
#8577=CARTESIAN_POINT('Origin',(-3.64952178519528,11.2640879581285,17.6));
#8578=CARTESIAN_POINT('',(-3.39952178519528,11.2640879581285,16.6));
#8579=CARTESIAN_POINT('',(-3.89952178519528,11.2640879581285,16.6));
#8580=CARTESIAN_POINT('Origin',(-3.64952178519528,11.2640879581285,16.6));
#8581=CARTESIAN_POINT('Ctrl Pts',(-3.39952178519528,11.2640879581285,16.6));
#8582=CARTESIAN_POINT('Ctrl Pts',(-3.39952178519528,11.2597806646461,16.5977092724426));
#8583=CARTESIAN_POINT('Ctrl Pts',(-3.39955324129755,11.2554410535254,16.5954788663774));
#8584=CARTESIAN_POINT('Ctrl Pts',(-3.40014364770956,11.2127459875283,16.5742560748851));
#8585=CARTESIAN_POINT('Ctrl Pts',(-3.40282286847409,11.1716935753448,16.559542959919));
#8586=CARTESIAN_POINT('Ctrl Pts',(-3.40690999909243,11.1298891387388,16.5481972195909));
#8587=CARTESIAN_POINT('Ctrl Pts',(-3.40698112962582,11.1291660315159,16.5480020646239));
#8588=CARTESIAN_POINT('Ctrl Pts',(-3.4081629902897,11.1172240770089,16.544797109728));
#8589=CARTESIAN_POINT('Ctrl Pts',(-3.409384175847,11.105936706496,16.5420298581508));
#8590=CARTESIAN_POINT('Ctrl Pts',(-3.41126371924574,11.089929722745,16.5384418503857));
#8591=CARTESIAN_POINT('Ctrl Pts',(-3.4118338437146,11.0852272650427,16.5374286265409));
#8592=CARTESIAN_POINT('Ctrl Pts',(-3.41287366194149,11.0769152925628,16.5357072275207));
#8593=CARTESIAN_POINT('Ctrl Pts',(-3.41333572893562,11.0733067646504,16.5349829852478));
#8594=CARTESIAN_POINT('Ctrl Pts',(-3.41433854491902,11.0656535215358,16.5334946079531));
#8595=CARTESIAN_POINT('Ctrl Pts',(-3.41488223353522,11.0616071709856,16.5327358435474));
#8596=CARTESIAN_POINT('Ctrl Pts',(-3.4162295106395,11.0518266202365,16.5309679692519));
#8597=CARTESIAN_POINT('Ctrl Pts',(-3.41704752686023,11.0460875459453,16.5299854641958));
#8598=CARTESIAN_POINT('Ctrl Pts',(-3.4199708406405,11.0262612081367,16.5267739133408));
#8599=CARTESIAN_POINT('Ctrl Pts',(-3.42222357481902,11.0121330333764,16.5248034466825));
#8600=CARTESIAN_POINT('Ctrl Pts',(-3.43123014519201,10.9599127812053,16.5186110231589));
#8601=CARTESIAN_POINT('Ctrl Pts',(-3.4391986219584,10.9214946617958,16.5162061142361));
#8602=CARTESIAN_POINT('Ctrl Pts',(-3.45515688387283,10.8586436195296,16.5154725363415));
#8603=CARTESIAN_POINT('Ctrl Pts',(-3.46228620261987,10.8336658536588,16.5160451884648));
#8604=CARTESIAN_POINT('Ctrl Pts',(-3.49512947595985,10.7324932763169,16.5219235534991));
#8605=CARTESIAN_POINT('Ctrl Pts',(-3.52630916660788,10.6660472824376,16.5341985199053));
#8606=CARTESIAN_POINT('Ctrl Pts',(-3.59133594943102,10.5724026680879,16.5639151059098));
#8607=CARTESIAN_POINT('Ctrl Pts',(-3.62203715988421,10.5415254901727,16.5791986989673));
#8608=CARTESIAN_POINT('Ctrl Pts',(-3.67499828617909,10.506956937443,16.605627659773));
#8609=CARTESIAN_POINT('Ctrl Pts',(-3.69704039179924,10.4980988346278,16.6166575639151));
#8610=CARTESIAN_POINT('Ctrl Pts',(-3.73479375210779,10.4922551407825,16.6350648852536));
#8611=CARTESIAN_POINT('Ctrl Pts',(-3.75139876442454,10.4929258201185,16.6429988757827));
#8612=CARTESIAN_POINT('Ctrl Pts',(-3.78199607956949,10.501731549649,16.6569651923278));
#8613=CARTESIAN_POINT('Ctrl Pts',(-3.79535203986082,10.5088054563803,16.6627780404676));
#8614=CARTESIAN_POINT('Ctrl Pts',(-3.82105390005994,10.5293269577824,16.6732083185761));
#8615=CARTESIAN_POINT('Ctrl Pts',(-3.83248647058025,10.5428683869631,16.677362768157));
#8616=CARTESIAN_POINT('Ctrl Pts',(-3.85612750484055,10.5800246546226,16.6848437491615));
#8617=CARTESIAN_POINT('Ctrl Pts',(-3.86624809413459,10.6053078595428,16.686910649375));
#8618=CARTESIAN_POINT('Ctrl Pts',(-3.88756792802042,10.6782927145015,16.6888104810606));
#8619=CARTESIAN_POINT('Ctrl Pts',(-3.89396521465656,10.7328116182588,16.6853604690573));
#8620=CARTESIAN_POINT('Ctrl Pts',(-3.90307097190431,10.9018817770723,16.6690502405298));
#8621=CARTESIAN_POINT('Ctrl Pts',(-3.89916166722153,11.1142796138527,16.6427595546923));
#8622=CARTESIAN_POINT('Ctrl Pts',(-3.89951831852135,11.258896367419,16.6015112866721));
#8623=CARTESIAN_POINT('Ctrl Pts',(-3.89952178519528,11.261493424974,16.6007604391535));
#8624=CARTESIAN_POINT('Ctrl Pts',(-3.89952178519528,11.2640879581285,16.6));
#8625=CARTESIAN_POINT('Ctrl Pts',(-3.89952178519528,11.2640879581285,16.6));
#8626=CARTESIAN_POINT('Ctrl Pts',(-3.89952178519528,11.100463340754,16.553125));
#8627=CARTESIAN_POINT('Ctrl Pts',(-3.98202611573229,10.7745871843551,16.459375));
#8628=CARTESIAN_POINT('Ctrl Pts',(-4.43258063114212,10.2697743643378,16.271875));
#8629=CARTESIAN_POINT('Ctrl Pts',(-5.34805346405984,10.1770907055197,16.0375));
#8630=CARTESIAN_POINT('Ctrl Pts',(-6.05333301021299,11.0351030238058,15.75625));
#8631=CARTESIAN_POINT('Ctrl Pts',(-5.7305291347766,12.0952484733215,15.475));
#8632=CARTESIAN_POINT('Ctrl Pts',(-4.67032720528385,12.41730825404,15.19375));
#8633=CARTESIAN_POINT('Ctrl Pts',(-3.81321563500956,11.71396418737,14.9125));
#8634=CARTESIAN_POINT('Ctrl Pts',(-3.92199706138937,10.6109219094395,14.63125));
#8635=CARTESIAN_POINT('Ctrl Pts',(-4.89949901982681,10.0883621413897,14.35));
#8636=CARTESIAN_POINT('Ctrl Pts',(-5.87710301444863,10.6109032023111,14.06875));
#8637=CARTESIAN_POINT('Ctrl Pts',(-5.98573321383868,11.7140106207574,13.7875));
#8638=CARTESIAN_POINT('Ctrl Pts',(-5.12889498447605,12.4172116991036,13.50625));
#8639=CARTESIAN_POINT('Ctrl Pts',(-4.06816558640322,12.095441826144,13.225));
#8640=CARTESIAN_POINT('Ctrl Pts',(-3.74640046021744,11.0347181280085,12.94375));
#8641=CARTESIAN_POINT('Ctrl Pts',(-4.44959545666081,10.177870497758,12.6625));
#8642=CARTESIAN_POINT('Ctrl Pts',(-5.55271322406204,10.2865183309037,12.38125));
#8643=CARTESIAN_POINT('Ctrl Pts',(-6.07523468001534,11.2640879581285,12.1));
#8644=CARTESIAN_POINT('Ctrl Pts',(-5.55271322406204,12.2416575853533,11.81875));
#8645=CARTESIAN_POINT('Ctrl Pts',(-4.44959545666081,12.3503054184991,11.5375));
#8646=CARTESIAN_POINT('Ctrl Pts',(-3.74640046021743,11.4934577882485,11.25625));
#8647=CARTESIAN_POINT('Ctrl Pts',(-4.06816558640323,10.432734090113,10.975));
#8648=CARTESIAN_POINT('Ctrl Pts',(-5.12889498447604,10.1109642171534,10.69375));
#8649=CARTESIAN_POINT('Ctrl Pts',(-5.98573321383869,10.8141652954996,10.4125));
#8650=CARTESIAN_POINT('Ctrl Pts',(-5.87710301444862,11.9172727139459,10.13125));
#8651=CARTESIAN_POINT('Ctrl Pts',(-4.89949901982682,12.4398137748673,9.85));
#8652=CARTESIAN_POINT('Ctrl Pts',(-3.92199706138938,11.9172540068175,9.56875));
#8653=CARTESIAN_POINT('Ctrl Pts',(-3.81321563500956,10.8142117288869,9.2875));
#8654=CARTESIAN_POINT('Ctrl Pts',(-4.67032720528385,10.110867662217,9.00625));
#8655=CARTESIAN_POINT('Ctrl Pts',(-5.73052913477659,10.4329274429355,8.725));
#8656=CARTESIAN_POINT('Ctrl Pts',(-6.05333301021299,11.4930728924512,8.44374999999999));
#8657=CARTESIAN_POINT('Ctrl Pts',(-5.34805346405984,12.3510852107373,8.16250000000001));
#8658=CARTESIAN_POINT('Ctrl Pts',(-4.43258063114213,12.2584015519192,7.92812499999999));
#8659=CARTESIAN_POINT('Ctrl Pts',(-3.98202611573229,11.7535887319019,7.740625));
#8660=CARTESIAN_POINT('Ctrl Pts',(-3.89952178519528,11.427712575503,7.646875));
#8661=CARTESIAN_POINT('Ctrl Pts',(-3.89952178519528,11.2640879581285,7.6));
#8662=CARTESIAN_POINT('Ctrl Pts',(-3.89952178519528,11.2640879581285,16.5439001311859));
#8663=CARTESIAN_POINT('Ctrl Pts',(-3.89952178519528,11.1005177695264,16.4970251311859));
#8664=CARTESIAN_POINT('Ctrl Pts',(-3.98203954157123,10.7745703060467,16.4032751311859));
#8665=CARTESIAN_POINT('Ctrl Pts',(-4.43255286964902,10.2698405453218,16.2157751311859));
#8666=CARTESIAN_POINT('Ctrl Pts',(-5.34806550647335,10.1770785267943,15.9814001311859));
#8667=CARTESIAN_POINT('Ctrl Pts',(-6.05330687653147,11.0351202247863,15.7001501311859));
#8668=CARTESIAN_POINT('Ctrl Pts',(-5.73052148986863,12.0952292689555,15.4189001311859));
#8669=CARTESIAN_POINT('Ctrl Pts',(-4.67032825737134,12.4172947840889,15.1376501311859));
#8670=CARTESIAN_POINT('Ctrl Pts',(-3.81323281431783,11.7139557792958,14.8564001311859));
#8671=CARTESIAN_POINT('Ctrl Pts',(-3.92201086686978,10.6109324328155,14.5751501311859));
#8672=CARTESIAN_POINT('Ctrl Pts',(-4.89949932136982,10.0883790058937,14.2939001311859));
#8673=CARTESIAN_POINT('Ctrl Pts',(-5.87708846051385,10.6109130556342,14.0126501311859));
#8674=CARTESIAN_POINT('Ctrl Pts',(-5.98571728919321,11.7140038758466,13.7314001311859));
#8675=CARTESIAN_POINT('Ctrl Pts',(-5.12889156632292,12.4171947705987,13.4501501311859));
#8676=CARTESIAN_POINT('Ctrl Pts',(-4.06817785358609,12.0954295490545,13.1689001311859));
#8677=CARTESIAN_POINT('Ctrl Pts',(-3.74641743755984,11.0347215219131,12.8876501311859));
#8678=CARTESIAN_POINT('Ctrl Pts',(-4.44960209025997,10.1778864924967,12.6064001311859));
#8679=CARTESIAN_POINT('Ctrl Pts',(-5.55270359818498,10.2865327351104,12.3251501311859));
#8680=CARTESIAN_POINT('Ctrl Pts',(-6.07521736228489,11.2640879581285,12.0439001311859));
#8681=CARTESIAN_POINT('Ctrl Pts',(-5.55270359818497,12.2416431811466,11.7626501311859));
#8682=CARTESIAN_POINT('Ctrl Pts',(-4.44960209025998,12.3502894237603,11.4814001311859));
#8683=CARTESIAN_POINT('Ctrl Pts',(-3.74641743755983,11.4934543943439,11.2001501311859));
#8684=CARTESIAN_POINT('Ctrl Pts',(-4.0681778535861,10.4327463672025,10.9189001311859));
#8685=CARTESIAN_POINT('Ctrl Pts',(-5.12889156632293,10.1109811456583,10.6376501311859));
#8686=CARTESIAN_POINT('Ctrl Pts',(-5.98571728919321,10.8141720404104,10.3564001311859));
#8687=CARTESIAN_POINT('Ctrl Pts',(-5.87708846051386,11.9172628606228,10.0751501311859));
#8688=CARTESIAN_POINT('Ctrl Pts',(-4.89949932136981,12.4397969103633,9.79390013118588));
#8689=CARTESIAN_POINT('Ctrl Pts',(-3.92201086686979,11.9172434834415,9.51265013118591));
#8690=CARTESIAN_POINT('Ctrl Pts',(-3.81323281431782,10.8142201369612,9.23140013118588));
#8691=CARTESIAN_POINT('Ctrl Pts',(-4.67032825737135,10.1108811321681,8.95015013118591));
#8692=CARTESIAN_POINT('Ctrl Pts',(-5.73052148986861,10.4329466473015,8.66890013118588));
#8693=CARTESIAN_POINT('Ctrl Pts',(-6.05330687653148,11.4930556914707,8.3876501311859));
#8694=CARTESIAN_POINT('Ctrl Pts',(-5.34806550647334,12.3510973894627,8.10640013118589));
#8695=CARTESIAN_POINT('Ctrl Pts',(-4.43255286964902,12.2583353709352,7.87202513118589));
#8696=CARTESIAN_POINT('Ctrl Pts',(-3.98203954157123,11.7536056102103,7.6845251311859));
#8697=CARTESIAN_POINT('Ctrl Pts',(-3.89952178519528,11.4276581467306,7.59077513118589));
#8698=CARTESIAN_POINT('Ctrl Pts',(-3.89952178519528,11.2640879581285,7.54390013118589));
#8699=CARTESIAN_POINT('Ctrl Pts',(-3.87336950513992,11.2640879581285,16.4693438123938));
#8700=CARTESIAN_POINT('Ctrl Pts',(-3.87336950513992,11.0961655481765,16.4224688123938));
#8701=CARTESIAN_POINT('Ctrl Pts',(-3.95802691518839,10.7617914019627,16.3287188123938));
#8702=CARTESIAN_POINT('Ctrl Pts',(-4.42037856051485,10.2437481371936,16.1412188123938));
#8703=CARTESIAN_POINT('Ctrl Pts',(-5.35977946696098,10.1486674187998,15.9068438123938));
#8704=CARTESIAN_POINT('Ctrl Pts',(-6.08351675236037,11.0291086562651,15.6255938123938));
#8705=CARTESIAN_POINT('Ctrl Pts',(-5.75226448923586,12.1169917912308,15.3443438123938));
#8706=CARTESIAN_POINT('Ctrl Pts',(-4.66433288422069,12.4474722061341,15.0630938123938));
#8707=CARTESIAN_POINT('Ctrl Pts',(-3.78480037035456,11.7257323553314,14.7818438123938));
#8708=CARTESIAN_POINT('Ctrl Pts',(-3.89642783422015,10.5938365249336,14.5005938123939));
#8709=CARTESIAN_POINT('Ctrl Pts',(-4.8994983212158,10.0576084563578,14.2193438123938));
#8710=CARTESIAN_POINT('Ctrl Pts',(-5.90267397562595,10.5938175579892,13.9380938123938));
#8711=CARTESIAN_POINT('Ctrl Pts',(-6.01414557172786,11.7257794336104,13.6568438123938));
#8712=CARTESIAN_POINT('Ctrl Pts',(-5.13489478695554,12.4473743102335,13.3755938123938));
#8713=CARTESIAN_POINT('Ctrl Pts',(-4.0464195261301,12.1171878288539,13.0943438123938));
#8714=CARTESIAN_POINT('Ctrl Pts',(-3.71623789555002,11.0287184219426,12.8130938123938));
#8715=CARTESIAN_POINT('Ctrl Pts',(-4.43782658604776,10.1494579581263,12.5318438123938));
#8716=CARTESIAN_POINT('Ctrl Pts',(-5.56979896528612,10.260947724411,12.2505938123938));
#8717=CARTESIAN_POINT('Ctrl Pts',(-6.10598818228894,11.2640879581285,11.9693438123938));
#8718=CARTESIAN_POINT('Ctrl Pts',(-5.56979896528612,12.267228191846,11.6880938123938));
#8719=CARTESIAN_POINT('Ctrl Pts',(-4.43782658604776,12.3787179581308,11.4068438123938));
#8720=CARTESIAN_POINT('Ctrl Pts',(-3.71623789555002,11.4994574943143,11.1255938123938));
#8721=CARTESIAN_POINT('Ctrl Pts',(-4.0464195261301,10.4109880874031,10.8443438123939));
#8722=CARTESIAN_POINT('Ctrl Pts',(-5.13489478695554,10.0808016060235,10.5630938123938));
#8723=CARTESIAN_POINT('Ctrl Pts',(-6.01414557172786,10.8023964826466,10.2818438123938));
#8724=CARTESIAN_POINT('Ctrl Pts',(-5.90267397562594,11.9343583582678,10.0005938123938));
#8725=CARTESIAN_POINT('Ctrl Pts',(-4.89949832121581,12.4705674598992,9.71934381239383));
#8726=CARTESIAN_POINT('Ctrl Pts',(-3.89642783422016,11.9343393913234,9.43809381239383));
#8727=CARTESIAN_POINT('Ctrl Pts',(-3.78480037035456,10.8024435609256,9.15684381239382));
#8728=CARTESIAN_POINT('Ctrl Pts',(-4.66433288422068,10.0807037101229,8.87559381239384));
#8729=CARTESIAN_POINT('Ctrl Pts',(-5.75226448923587,10.4111841250261,8.59434381239382));
#8730=CARTESIAN_POINT('Ctrl Pts',(-6.08351675236036,11.4990672599919,8.31309381239383));
#8731=CARTESIAN_POINT('Ctrl Pts',(-5.35977946696099,12.3795084974572,8.03184381239384));
#8732=CARTESIAN_POINT('Ctrl Pts',(-4.42037856051485,12.2844277790635,7.79746881239382));
#8733=CARTESIAN_POINT('Ctrl Pts',(-3.95802691518839,11.7663845142943,7.60996881239383));
#8734=CARTESIAN_POINT('Ctrl Pts',(-3.87336950513992,11.4320103680805,7.51621881239383));
#8735=CARTESIAN_POINT('Ctrl Pts',(-3.87336950513992,11.2640879581285,7.46934381239383));
#8736=CARTESIAN_POINT('Ctrl Pts',(-3.79339036013458,11.2640879581285,16.3896607060098));
#8737=CARTESIAN_POINT('Ctrl Pts',(-3.79339036013458,11.0831088802229,16.3427857060098));
#8738=CARTESIAN_POINT('Ctrl Pts',(-3.8846537686712,10.7226322800334,16.2490357060098));
#8739=CARTESIAN_POINT('Ctrl Pts',(-4.38301776128431,10.1642601287568,16.0615357060098));
#8740=CARTESIAN_POINT('Ctrl Pts',(-5.39565926012194,10.0617236200811,15.8271607060098));
#8741=CARTESIAN_POINT('Ctrl Pts',(-6.17578323657063,11.0108040827547,15.5459107060098));
#8742=CARTESIAN_POINT('Ctrl Pts',(-5.81872354841958,12.1834567527021,15.2646607060098));
#8743=CARTESIAN_POINT('Ctrl Pts',(-4.6460026754234,12.5396983825077,14.9834107060098));
#8744=CARTESIAN_POINT('Ctrl Pts',(-3.69792796710343,11.7617084542898,14.7021607060098));
#8745=CARTESIAN_POINT('Ctrl Pts',(-3.81825382373765,10.5416026416254,14.4209107060098));
#8746=CARTESIAN_POINT('Ctrl Pts',(-4.8994966660506,9.96358417175727,14.1396607060098));
#8747=CARTESIAN_POINT('Ctrl Pts',(-5.98085209435916,10.5415818105476,13.8584107060098));
#8748=CARTESIAN_POINT('Ctrl Pts',(-6.10101108821724,11.761760159582,13.5771607060098));
#8749=CARTESIAN_POINT('Ctrl Pts',(-5.15323798227467,12.5395908649936,13.2959107060098));
#8750=CARTESIAN_POINT('Ctrl Pts',(-3.97993510456335,12.183672058567,13.0146607060098));
#8751=CARTESIAN_POINT('Ctrl Pts',(-3.62402156083799,11.0103754827702,12.7334107060098));
#8752=CARTESIAN_POINT('Ctrl Pts',(-4.40184550575446,10.0625919977156,12.4521607060099));
#8753=CARTESIAN_POINT('Ctrl Pts',(-5.62203537213207,10.1827704513763,12.1709107060098));
#8754=CARTESIAN_POINT('Ctrl Pts',(-6.20001118452041,11.2640879581285,11.8896607060099));
#8755=CARTESIAN_POINT('Ctrl Pts',(-5.62203537213207,12.3454054648807,11.6084107060098));
#8756=CARTESIAN_POINT('Ctrl Pts',(-4.40184550575447,12.4655839185415,11.3271607060098));
#8757=CARTESIAN_POINT('Ctrl Pts',(-3.62402156083798,11.5178004334867,11.0459107060098));
#8758=CARTESIAN_POINT('Ctrl Pts',(-3.97993510456335,10.34450385769,10.7646607060098));
#8759=CARTESIAN_POINT('Ctrl Pts',(-5.15323798227467,9.98858505126339,10.4834107060098));
#8760=CARTESIAN_POINT('Ctrl Pts',(-6.10101108821723,10.766415756675,10.2021607060098));
#8761=CARTESIAN_POINT('Ctrl Pts',(-5.98085209435917,11.9865941057094,9.92091070600982));
#8762=CARTESIAN_POINT('Ctrl Pts',(-4.89949666605059,12.5645917444997,9.63966070600984));
#8763=CARTESIAN_POINT('Ctrl Pts',(-3.81825382373766,11.9865732746316,9.35841070600983));
#8764=CARTESIAN_POINT('Ctrl Pts',(-3.69792796710343,10.7664674619671,9.07716070600983));
#8765=CARTESIAN_POINT('Ctrl Pts',(-4.64600267542341,9.98847753374938,8.79591070600983));
#8766=CARTESIAN_POINT('Ctrl Pts',(-5.81872354841957,10.3447191635549,8.51466070600983));
#8767=CARTESIAN_POINT('Ctrl Pts',(-6.17578323657063,11.5173718335023,8.23341070600984));
#8768=CARTESIAN_POINT('Ctrl Pts',(-5.39565926012194,12.4664522961759,7.95216070600983));
#8769=CARTESIAN_POINT('Ctrl Pts',(-4.38301776128432,12.3639157875002,7.71778570600983));
#8770=CARTESIAN_POINT('Ctrl Pts',(-3.8846537686712,11.8055436362236,7.53028570600983));
#8771=CARTESIAN_POINT('Ctrl Pts',(-3.79339036013458,11.4450670360341,7.43653570600983));
#8772=CARTESIAN_POINT('Ctrl Pts',(-3.79339036013458,11.2640879581285,7.38966070600983));
#8773=CARTESIAN_POINT('Ctrl Pts',(-3.68970487524127,11.2640879581285,16.3393272852701));
#8774=CARTESIAN_POINT('Ctrl Pts',(-3.68970487524127,11.0661279362491,16.2924522852701));
#8775=CARTESIAN_POINT('Ctrl Pts',(-3.78951897521615,10.6718829447944,16.1987022852701));
#8776=CARTESIAN_POINT('Ctrl Pts',(-4.33461061966199,10.0611454603422,16.0112022852701));
#8777=CARTESIAN_POINT('Ctrl Pts',(-5.44216206725399,9.9490212390312,15.7768272852701));
#8778=CARTESIAN_POINT('Ctrl Pts',(-6.2954241293124,10.9870567873906,15.4955772852701));
#8779=CARTESIAN_POINT('Ctrl Pts',(-5.90488911793673,12.2696414836945,15.2143272852701));
#8780=CARTESIAN_POINT('Ctrl Pts',(-4.62223822570157,12.6592744106758,14.9330772852701));
#8781=CARTESIAN_POINT('Ctrl Pts',(-3.58528891191358,11.8083564753633,14.6518272852701));
#8782=CARTESIAN_POINT('Ctrl Pts',(-3.71689478093803,10.4738758167534,14.3705772852701));
#8783=CARTESIAN_POINT('Ctrl Pts',(-4.89949422003833,9.84167368441925,14.0893272852701));
#8784=CARTESIAN_POINT('Ctrl Pts',(-6.08221720835516,10.4738532361703,13.8080772852701));
#8785=CARTESIAN_POINT('Ctrl Pts',(-6.213639966101,11.8084125231395,13.5268272852701));
#8786=CARTESIAN_POINT('Ctrl Pts',(-5.17702162369123,12.6591578633091,13.2455772852701));
#8787=CARTESIAN_POINT('Ctrl Pts',(-3.89373205270486,12.2698748715692,12.9643272852701));
#8788=CARTESIAN_POINT('Ctrl Pts',(-3.50445479916688,10.9865921975682,12.6830772852701));
#8789=CARTESIAN_POINT('Ctrl Pts',(-4.35519279368454,9.94996247453771,12.4018272852701));
#8790=CARTESIAN_POINT('Ctrl Pts',(-5.68976457489842,10.0814065828331,12.1205772852701));
#8791=CARTESIAN_POINT('Ctrl Pts',(-6.32192046066284,11.2640879581285,11.8393272852701));
#8792=CARTESIAN_POINT('Ctrl Pts',(-5.68976457489842,12.4467693334238,11.5580772852701));
#8793=CARTESIAN_POINT('Ctrl Pts',(-4.35519279368455,12.5782134417193,11.2768272852701));
#8794=CARTESIAN_POINT('Ctrl Pts',(-3.50445479916687,11.5415837186888,10.9955772852701));
#8795=CARTESIAN_POINT('Ctrl Pts',(-3.89373205270487,10.2583010446878,10.7143272852701));
#8796=CARTESIAN_POINT('Ctrl Pts',(-5.17702162369123,9.8690180529479,10.4330772852701));
#8797=CARTESIAN_POINT('Ctrl Pts',(-6.21363996610101,10.7197633931175,10.1518272852701));
#8798=CARTESIAN_POINT('Ctrl Pts',(-6.08221720835516,12.0543226800868,9.87057728527009));
#8799=CARTESIAN_POINT('Ctrl Pts',(-4.89949422003833,12.6865022318377,9.58932728527009));
#8800=CARTESIAN_POINT('Ctrl Pts',(-3.71689478093804,12.0543000995037,9.3080772852701));
#8801=CARTESIAN_POINT('Ctrl Pts',(-3.58528891191358,10.7198194408936,9.02682728527009));
#8802=CARTESIAN_POINT('Ctrl Pts',(-4.62223822570156,9.86890150558126,8.74557728527009));
#8803=CARTESIAN_POINT('Ctrl Pts',(-5.90488911793673,10.2585344325625,8.4643272852701));
#8804=CARTESIAN_POINT('Ctrl Pts',(-6.2954241293124,11.5411191288664,8.18307728527009));
#8805=CARTESIAN_POINT('Ctrl Pts',(-5.442162067254,12.5791546772258,7.9018272852701));
#8806=CARTESIAN_POINT('Ctrl Pts',(-4.33461061966199,12.4670304559148,7.66745228527008));
#8807=CARTESIAN_POINT('Ctrl Pts',(-3.78951897521615,11.8562929714626,7.4799522852701));
#8808=CARTESIAN_POINT('Ctrl Pts',(-3.68970487524127,11.4620479800079,7.38620228527009));
#8809=CARTESIAN_POINT('Ctrl Pts',(-3.68970487524127,11.2640879581285,7.33932728527009));
#8810=CARTESIAN_POINT('Ctrl Pts',(-3.53279772223055,11.2640879581285,16.3570673917264));
#8811=CARTESIAN_POINT('Ctrl Pts',(-3.53279772223055,11.0404597227958,16.3101923917264));
#8812=CARTESIAN_POINT('Ctrl Pts',(-3.64555873781947,10.5950750170041,16.2164423917264));
#8813=CARTESIAN_POINT('Ctrl Pts',(-4.26134132595788,9.90513742653932,16.0289423917264));
#8814=CARTESIAN_POINT('Ctrl Pts',(-5.51254114817169,9.7784623284684,15.7945673917264));
#8815=CARTESIAN_POINT('Ctrl Pts',(-6.47646264640105,10.9511292017956,15.5133173917264));
#8816=CARTESIAN_POINT('Ctrl Pts',(-6.03527932038454,12.4000545169874,15.2320673917264));
#8817=CARTESIAN_POINT('Ctrl Pts',(-4.58627606607664,12.8402215235162,14.9508173917264));
#8818=CARTESIAN_POINT('Ctrl Pts',(-3.41484149286839,11.878944399442,14.6695673917264));
#8819=CARTESIAN_POINT('Ctrl Pts',(-3.56351559500105,10.371390485815,14.3883173917264));
#8820=CARTESIAN_POINT('Ctrl Pts',(-4.89949067934314,9.65719564733918,14.1070673917264));
#8821=CARTESIAN_POINT('Ctrl Pts',(-6.23560518257789,10.3713649002786,13.8258173917264));
#8822=CARTESIAN_POINT('Ctrl Pts',(-6.38407265311657,11.879007905882,13.5445673917264));
#8823=CARTESIAN_POINT('Ctrl Pts',(-5.21301156395295,12.8400894663742,13.2633173917264));
#8824=CARTESIAN_POINT('Ctrl Pts',(-3.7632875939377,12.4003189635907,12.9820673917264));
#8825=CARTESIAN_POINT('Ctrl Pts',(-3.32352358026704,10.9506027834305,12.7008173917264));
#8826=CARTESIAN_POINT('Ctrl Pts',(-4.28459682416124,9.77952884838916,12.4195673917264));
#8827=CARTESIAN_POINT('Ctrl Pts',(-5.79225398305782,9.92802041348316,12.1383173917264));
#8828=CARTESIAN_POINT('Ctrl Pts',(-6.50639642307561,11.2640879581285,11.8570673917264));
#8829=CARTESIAN_POINT('Ctrl Pts',(-5.79225398305783,12.6001555027738,11.5758173917264));
#8830=CARTESIAN_POINT('Ctrl Pts',(-4.28459682416124,12.7486470678678,11.2945673917264));
#8831=CARTESIAN_POINT('Ctrl Pts',(-3.32352358026704,11.5775731328264,11.0133173917264));
#8832=CARTESIAN_POINT('Ctrl Pts',(-3.76328759393771,10.1278569526663,10.7320673917264));
#8833=CARTESIAN_POINT('Ctrl Pts',(-5.21301156395294,9.68808644988274,10.4508173917264));
#8834=CARTESIAN_POINT('Ctrl Pts',(-6.38407265311658,10.649168010375,10.1695673917264));
#8835=CARTESIAN_POINT('Ctrl Pts',(-6.23560518257789,12.1568110159784,9.88831739172645));
#8836=CARTESIAN_POINT('Ctrl Pts',(-4.89949067934315,12.8709802689178,9.60706739172643));
#8837=CARTESIAN_POINT('Ctrl Pts',(-3.56351559500104,12.156785430442,9.32581739172646));
#8838=CARTESIAN_POINT('Ctrl Pts',(-3.41484149286839,10.649231516815,9.04456739172643));
#8839=CARTESIAN_POINT('Ctrl Pts',(-4.58627606607664,9.68795439274076,8.76331739172645));
#8840=CARTESIAN_POINT('Ctrl Pts',(-6.03527932038453,10.1281213992696,8.48206739172642));
#8841=CARTESIAN_POINT('Ctrl Pts',(-6.47646264640105,11.5770467144613,8.20081739172645));
#8842=CARTESIAN_POINT('Ctrl Pts',(-5.51254114817169,12.7497135877886,7.91956739172644));
#8843=CARTESIAN_POINT('Ctrl Pts',(-4.26134132595789,12.6230384897176,7.68519239172645));
#8844=CARTESIAN_POINT('Ctrl Pts',(-3.64555873781947,11.9331008992529,7.49769239172644));
#8845=CARTESIAN_POINT('Ctrl Pts',(-3.53279772223055,11.4877161934612,7.40394239172644));
#8846=CARTESIAN_POINT('Ctrl Pts',(-3.53279772223055,11.2640879581285,7.35706739172644));
#8847=CARTESIAN_POINT('Ctrl Pts',(-3.39185155845223,11.2640879581285,16.4968402459044));
#8848=CARTESIAN_POINT('Ctrl Pts',(-3.39185155845223,11.0174025726682,16.4499652459044));
#8849=CARTESIAN_POINT('Ctrl Pts',(-3.51624250389027,10.5260801755509,16.3562152459045));
#8850=CARTESIAN_POINT('Ctrl Pts',(-4.19552515420369,9.76499895566937,16.1687152459044));
#8851=CARTESIAN_POINT('Ctrl Pts',(-5.57576109867319,9.62525309184065,15.9343402459045));
#8852=CARTESIAN_POINT('Ctrl Pts',(-6.63908545779677,10.9188562692688,15.6530902459045));
#8853=CARTESIAN_POINT('Ctrl Pts',(-6.15240590036416,12.5172015993995,15.3718402459044));
#8854=CARTESIAN_POINT('Ctrl Pts',(-4.55397206809218,13.0027622351084,15.0905902459045));
#8855=CARTESIAN_POINT('Ctrl Pts',(-3.2617324218044,11.9423519384361,14.8093402459044));
#8856=CARTESIAN_POINT('Ctrl Pts',(-3.42573853180317,10.2793302253054,14.5280902459045));
#8857=CARTESIAN_POINT('Ctrl Pts',(-4.89948749897295,9.49148318774154,14.2468402459044));
#8858=CARTESIAN_POINT('Ctrl Pts',(-6.37339013970644,10.2793019401391,13.9655902459045));
#8859=CARTESIAN_POINT('Ctrl Pts',(-6.53716849138144,11.9424221456894,13.6843402459045));
#8860=CARTESIAN_POINT('Ctrl Pts',(-5.24534051542964,13.0026162440886,13.4030902459044));
#8861=CARTESIAN_POINT('Ctrl Pts',(-3.64611227912762,12.5174939489564,13.1218402459045));
#8862=CARTESIAN_POINT('Ctrl Pts',(-3.16099714766513,10.9182743045467,12.8405902459044));
#8863=CARTESIAN_POINT('Ctrl Pts',(-4.22118205720403,9.62643216655873,12.5593402459045));
#8864=CARTESIAN_POINT('Ctrl Pts',(-5.88431790650939,9.79023707755347,12.2780902459044));
#8865=CARTESIAN_POINT('Ctrl Pts',(-6.67210701881104,11.2640879581285,11.9968402459045));
#8866=CARTESIAN_POINT('Ctrl Pts',(-5.88431790650938,12.7379388387035,11.7155902459044));
#8867=CARTESIAN_POINT('Ctrl Pts',(-4.22118205720405,12.9017437496983,11.4343402459045));
#8868=CARTESIAN_POINT('Ctrl Pts',(-3.16099714766512,11.6099016117103,11.1530902459044));
#8869=CARTESIAN_POINT('Ctrl Pts',(-3.64611227912763,10.0106819673006,10.8718402459045));
#8870=CARTESIAN_POINT('Ctrl Pts',(-5.24534051542964,9.52555967216844,10.5905902459044));
#8871=CARTESIAN_POINT('Ctrl Pts',(-6.53716849138144,10.5857537705676,10.3093402459045));
#8872=CARTESIAN_POINT('Ctrl Pts',(-6.37339013970643,12.2488739761179,10.0280902459045));
#8873=CARTESIAN_POINT('Ctrl Pts',(-4.89948749897296,13.0366927285155,9.74684024590444));
#8874=CARTESIAN_POINT('Ctrl Pts',(-3.42573853180317,12.2488456909516,9.46559024590447));
#8875=CARTESIAN_POINT('Ctrl Pts',(-3.26173242180439,10.585823977821,9.18434024590444));
#8876=CARTESIAN_POINT('Ctrl Pts',(-4.55397206809218,9.52541368114862,8.90309024590446));
#8877=CARTESIAN_POINT('Ctrl Pts',(-6.15240590036416,10.0109743168575,8.62184024590445));
#8878=CARTESIAN_POINT('Ctrl Pts',(-6.63908545779677,11.6093196469882,8.34059024590444));
#8879=CARTESIAN_POINT('Ctrl Pts',(-5.5757610986732,12.9029228244164,8.05934024590446));
#8880=CARTESIAN_POINT('Ctrl Pts',(-4.19552515420369,12.7631769605876,7.82496524590443));
#8881=CARTESIAN_POINT('Ctrl Pts',(-3.51624250389027,12.0020957407061,7.63746524590445));
#8882=CARTESIAN_POINT('Ctrl Pts',(-3.39185155845223,11.5107733435888,7.54371524590445));
#8883=CARTESIAN_POINT('Ctrl Pts',(-3.39185155845223,11.2640879581285,7.49684024590445));
#8884=CARTESIAN_POINT('Ctrl Pts',(-3.39169253443538,11.2640879581285,16.7239318526328));
#8885=CARTESIAN_POINT('Ctrl Pts',(-3.39169253443538,11.0173582841831,16.6770568526328));
#8886=CARTESIAN_POINT('Ctrl Pts',(-3.51609209385211,10.5260079981351,16.5833068526328));
#8887=CARTESIAN_POINT('Ctrl Pts',(-4.19546021709497,9.76481862322427,16.3958068526328));
#8888=CARTESIAN_POINT('Ctrl Pts',(-5.57582838411809,9.62508432078666,16.1614318526328));
#8889=CARTESIAN_POINT('Ctrl Pts',(-6.63927771288993,10.9188140819009,15.8801818526328));
#8890=CARTESIAN_POINT('Ctrl Pts',(-6.15254061639523,12.5173402195548,15.5989318526328));
#8891=CARTESIAN_POINT('Ctrl Pts',(-4.55393526753129,13.0029501458291,15.3176818526328));
#8892=CARTESIAN_POINT('Ctrl Pts',(-3.26155390704704,11.9424263016113,15.0364318526328));
#8893=CARTESIAN_POINT('Ctrl Pts',(-3.42557844828242,10.2792228241956,14.7551818526328));
#8894=CARTESIAN_POINT('Ctrl Pts',(-4.89948739414409,9.4912905587692,14.4739318526328));
#8895=CARTESIAN_POINT('Ctrl Pts',(-6.37355048342092,10.2791947609481,14.1926818526328));
#8896=CARTESIAN_POINT('Ctrl Pts',(-6.53734656996609,11.9424959580315,13.9114318526328));
#8897=CARTESIAN_POINT('Ctrl Pts',(-5.24537813853149,13.002805300269,13.6301818526328));
#8898=CARTESIAN_POINT('Ctrl Pts',(-3.64597595622047,12.5176302748179,13.3489318526328));
#8899=CARTESIAN_POINT('Ctrl Pts',(-3.16080807547727,10.9182366901193,13.0676818526328));
#8900=CARTESIAN_POINT('Ctrl Pts',(-4.22110828163903,9.62625406348905,12.7864318526328));
#8901=CARTESIAN_POINT('Ctrl Pts',(-5.8844250104241,9.79007678593805,12.5051818526328));
#8902=CARTESIAN_POINT('Ctrl Pts',(-6.67229979784745,11.2640879581285,12.2239318526328));
#8903=CARTESIAN_POINT('Ctrl Pts',(-5.8844250104241,12.7380991303189,11.9426818526328));
#8904=CARTESIAN_POINT('Ctrl Pts',(-4.22110828163903,12.9019218527679,11.6614318526328));
#8905=CARTESIAN_POINT('Ctrl Pts',(-3.16080807547727,11.6099392261377,11.3801818526328));
#8906=CARTESIAN_POINT('Ctrl Pts',(-3.64597595622048,10.0105456414391,11.0989318526328));
#8907=CARTESIAN_POINT('Ctrl Pts',(-5.24537813853148,9.52537061598797,10.8176818526328));
#8908=CARTESIAN_POINT('Ctrl Pts',(-6.5373465699661,10.5856799582255,10.5364318526328));
#8909=CARTESIAN_POINT('Ctrl Pts',(-6.37355048342092,12.2489811553089,10.2551818526328));
#8910=CARTESIAN_POINT('Ctrl Pts',(-4.8994873941441,13.0368853574878,9.97393185263282));
#8911=CARTESIAN_POINT('Ctrl Pts',(-3.42557844828242,12.2489530920614,9.69268185263279));
#8912=CARTESIAN_POINT('Ctrl Pts',(-3.26155390704705,10.5857496146457,9.41143185263281));
#8913=CARTESIAN_POINT('Ctrl Pts',(-4.55393526753128,9.52522577042787,9.13018185263281));
#8914=CARTESIAN_POINT('Ctrl Pts',(-6.15254061639523,10.0108356967022,8.84893185263278));
#8915=CARTESIAN_POINT('Ctrl Pts',(-6.63927771288993,11.6093618343561,8.56768185263281));
#8916=CARTESIAN_POINT('Ctrl Pts',(-5.57582838411809,12.9030915954703,8.28643185263279));
#8917=CARTESIAN_POINT('Ctrl Pts',(-4.19546021709497,12.7633572930327,8.05205685263281));
#8918=CARTESIAN_POINT('Ctrl Pts',(-3.51609209385211,12.0021679181219,7.86455685263281));
#8919=CARTESIAN_POINT('Ctrl Pts',(-3.39169253443538,11.5108176320739,7.77080685263281));
#8920=CARTESIAN_POINT('Ctrl Pts',(-3.39169253443538,11.2640879581285,7.72393185263281));
#8921=CARTESIAN_POINT('Ctrl Pts',(-3.58586091972906,11.2640879581285,16.8792236164212));
#8922=CARTESIAN_POINT('Ctrl Pts',(-3.58586091972906,11.0491619105831,16.8323486164212));
#8923=CARTESIAN_POINT('Ctrl Pts',(-3.69424886155145,10.6210433711399,16.7385986164213));
#8924=CARTESIAN_POINT('Ctrl Pts',(-4.28610864698902,9.95792289030335,16.5510986164212));
#8925=CARTESIAN_POINT('Ctrl Pts',(-5.48874499113504,9.83613746089765,16.3167236164213));
#8926=CARTESIAN_POINT('Ctrl Pts',(-6.41522825428506,10.9632861137281,16.0354736164213));
#8927=CARTESIAN_POINT('Ctrl Pts',(-5.99118064031058,12.3559435166106,15.7542236164212));
#8928=CARTESIAN_POINT('Ctrl Pts',(-4.59843824494916,12.7790230813754,15.4729736164213));
#8929=CARTESIAN_POINT('Ctrl Pts',(-3.47249060193688,11.8550694784638,15.1917236164212));
#8930=CARTESIAN_POINT('Ctrl Pts',(-3.61539119000279,10.406053381894,14.9104736164213));
#8931=CARTESIAN_POINT('Ctrl Pts',(-4.89949199672205,9.71958953564843,14.6292236164212));
#8932=CARTESIAN_POINT('Ctrl Pts',(-6.18372631773713,10.4060285459761,14.3479736164213));
#8933=CARTESIAN_POINT('Ctrl Pts',(-6.3264290253672,11.8551311242623,14.0667236164213));
#8934=CARTESIAN_POINT('Ctrl Pts',(-5.20083904874642,12.7788948932607,13.7854736164212));
#8935=CARTESIAN_POINT('Ctrl Pts',(-3.80740646165742,12.3562002159562,13.5042236164213));
#8936=CARTESIAN_POINT('Ctrl Pts',(-3.38471804289437,10.9627751110632,13.2229736164213));
#8937=CARTESIAN_POINT('Ctrl Pts',(-4.30847375993061,9.83717282162548,12.9417236164213));
#8938=CARTESIAN_POINT('Ctrl Pts',(-5.75759006523555,9.97989860837387,12.6604736164212));
#8939=CARTESIAN_POINT('Ctrl Pts',(-6.44400305605043,11.2640879581285,12.3792236164213));
#8940=CARTESIAN_POINT('Ctrl Pts',(-5.75759006523555,12.5482773078831,12.0979736164212));
#8941=CARTESIAN_POINT('Ctrl Pts',(-4.30847375993062,12.6910030946315,11.8167236164213));
#8942=CARTESIAN_POINT('Ctrl Pts',(-3.38471804289437,11.5654008051937,11.5354736164212));
#8943=CARTESIAN_POINT('Ctrl Pts',(-3.80740646165742,10.1719757003009,11.2542236164213));
#8944=CARTESIAN_POINT('Ctrl Pts',(-5.20083904874642,9.74928102299629,10.9729736164213));
#8945=CARTESIAN_POINT('Ctrl Pts',(-6.3264290253672,10.6730447919947,10.6917236164212));
#8946=CARTESIAN_POINT('Ctrl Pts',(-6.18372631773713,12.1221473702809,10.4104736164213));
#8947=CARTESIAN_POINT('Ctrl Pts',(-4.89949199672205,12.8085863806086,10.1292236164212));
#8948=CARTESIAN_POINT('Ctrl Pts',(-3.61539119000279,12.122122534363,9.84797361642129));
#8949=CARTESIAN_POINT('Ctrl Pts',(-3.47249060193688,10.6731064377931,9.56672361642123));
#8950=CARTESIAN_POINT('Ctrl Pts',(-4.59843824494915,9.7491528348816,9.28547361642126));
#8951=CARTESIAN_POINT('Ctrl Pts',(-5.99118064031059,10.1722323996464,9.00422361642126));
#8952=CARTESIAN_POINT('Ctrl Pts',(-6.41522825428506,11.5648898025289,8.72297361642125));
#8953=CARTESIAN_POINT('Ctrl Pts',(-5.48874499113504,12.6920384553594,8.44172361642126));
#8954=CARTESIAN_POINT('Ctrl Pts',(-4.28610864698902,12.5702530259537,8.20734861642126));
#8955=CARTESIAN_POINT('Ctrl Pts',(-3.69424886155145,11.9071325451172,8.01984861642125));
#8956=CARTESIAN_POINT('Ctrl Pts',(-3.58586091972906,11.4790140056738,7.92609861642125));
#8957=CARTESIAN_POINT('Ctrl Pts',(-3.58586091972906,11.2640879581285,7.87922361642125));
#8958=CARTESIAN_POINT('Ctrl Pts',(-3.82797537247149,11.2640879581285,16.8235757346037));
#8959=CARTESIAN_POINT('Ctrl Pts',(-3.82797537247149,11.0887036859235,16.7767007346037));
#8960=CARTESIAN_POINT('Ctrl Pts',(-3.91636954304832,10.7395815643351,16.6829507346037));
#8961=CARTESIAN_POINT('Ctrl Pts',(-4.39919964857289,10.1985704709434,16.4954507346037));
#8962=CARTESIAN_POINT('Ctrl Pts',(-5.38013259241044,10.0993317882042,16.2610757346037));
#8963=CARTESIAN_POINT('Ctrl Pts',(-6.13590946417683,11.0187032552064,15.9798257346037));
#8964=CARTESIAN_POINT('Ctrl Pts',(-5.78999215982685,12.1547336916928,15.6985757346036));
#8965=CARTESIAN_POINT('Ctrl Pts',(-4.65392813273036,12.4998301210104,15.4173257346037));
#8966=CARTESIAN_POINT('Ctrl Pts',(-3.73547762992698,11.7461593897193,15.1360757346036));
#8967=CARTESIAN_POINT('Ctrl Pts',(-3.85204525622676,10.5641799938609,14.8548257346037));
#8968=CARTESIAN_POINT('Ctrl Pts',(-4.89949709797062,10.004226785903,14.5735757346036));
#8969=CARTESIAN_POINT('Ctrl Pts',(-5.94705958981123,10.5641605995425,14.2923257346037));
#8970=CARTESIAN_POINT('Ctrl Pts',(-6.06346322250255,11.7462075287867,14.0110757346037));
#8971=CARTESIAN_POINT('Ctrl Pts',(-5.1453091362317,12.4997300193532,13.7298257346037));
#8972=CARTESIAN_POINT('Ctrl Pts',(-4.00867310996093,12.154934145456,13.4485757346037));
#8973=CARTESIAN_POINT('Ctrl Pts',(-3.66388226535769,11.0183042408718,13.1673257346037));
#8974=CARTESIAN_POINT('Ctrl Pts',(-4.41739839453505,10.1001399894206,12.8860757346037));
#8975=CARTESIAN_POINT('Ctrl Pts',(-5.59945608391935,10.2165627311483,12.6048257346037));
#8976=CARTESIAN_POINT('Ctrl Pts',(-6.15936955148513,11.2640879581285,12.3235757346037));
#8977=CARTESIAN_POINT('Ctrl Pts',(-5.59945608391935,12.3116131851086,12.0423257346036));
#8978=CARTESIAN_POINT('Ctrl Pts',(-4.41739839453506,12.4280359268364,11.7610757346037));
#8979=CARTESIAN_POINT('Ctrl Pts',(-3.66388226535769,11.5098716753851,11.4798257346036));
#8980=CARTESIAN_POINT('Ctrl Pts',(-4.00867310996093,10.373241770801,11.1985757346037));
#8981=CARTESIAN_POINT('Ctrl Pts',(-5.14530913623169,10.0284458969038,10.9173257346037));
#8982=CARTESIAN_POINT('Ctrl Pts',(-6.06346322250255,10.7819683874703,10.6360757346037));
#8983=CARTESIAN_POINT('Ctrl Pts',(-5.94705958981124,11.9640153167145,10.3548257346037));
#8984=CARTESIAN_POINT('Ctrl Pts',(-4.89949709797062,12.523949130354,10.0735757346037));
#8985=CARTESIAN_POINT('Ctrl Pts',(-3.85204525622676,11.9639959223961,9.79232573460369));
#8986=CARTESIAN_POINT('Ctrl Pts',(-3.73547762992698,10.7820165265377,9.51107573460366));
#8987=CARTESIAN_POINT('Ctrl Pts',(-4.65392813273036,10.0283457952466,9.22982573460369));
#8988=CARTESIAN_POINT('Ctrl Pts',(-5.78999215982684,10.3734422245642,8.94857573460365));
#8989=CARTESIAN_POINT('Ctrl Pts',(-6.13590946417682,11.5094726610506,8.66732573460368));
#8990=CARTESIAN_POINT('Ctrl Pts',(-5.38013259241045,12.4288441280527,8.38607573460367));
#8991=CARTESIAN_POINT('Ctrl Pts',(-4.39919964857288,12.3296054453136,8.15170073460366));
#8992=CARTESIAN_POINT('Ctrl Pts',(-3.91636954304832,11.7885943519219,7.96420073460368));
#8993=CARTESIAN_POINT('Ctrl Pts',(-3.82797537247149,11.4394722303336,7.87045073460367));
#8994=CARTESIAN_POINT('Ctrl Pts',(-3.82797537247149,11.2640879581285,7.82357573460367));
#8995=CARTESIAN_POINT('Ctrl Pts',(-3.89952178519528,11.2640879581285,16.6747998250855));
#8996=CARTESIAN_POINT('Ctrl Pts',(-3.89952178519528,11.1005833965992,16.6279248250855));
#8997=CARTESIAN_POINT('Ctrl Pts',(-3.98205572967308,10.7745499551565,16.5341748250855));
#8998=CARTESIAN_POINT('Ctrl Pts',(-4.43251939644262,10.2699203425333,16.3466748250855));
#8999=CARTESIAN_POINT('Ctrl Pts',(-5.34808002652064,10.1770638423901,16.1122998250855));
#9000=CARTESIAN_POINT('Ctrl Pts',(-6.05327536604636,11.0351409647361,15.8310498250855));
#9001=CARTESIAN_POINT('Ctrl Pts',(-5.73051227207975,12.0952061134392,15.5497998250855));
#9002=CARTESIAN_POINT('Ctrl Pts',(-4.67032952591772,12.4172785427992,15.2685498250855));
#9003=CARTESIAN_POINT('Ctrl Pts',(-3.81325352813639,11.7139456413251,14.9872998250855));
#9004=CARTESIAN_POINT('Ctrl Pts',(-3.92202751272141,10.610945121295,14.7060498250855));
#9005=CARTESIAN_POINT('Ctrl Pts',(-4.89949968495297,10.0883993401394,14.4247998250855));
#9006=CARTESIAN_POINT('Ctrl Pts',(-5.87707091221916,10.6109249362026,14.1435498250855));
#9007=CARTESIAN_POINT('Ctrl Pts',(-5.98569808817465,11.7139957432225,13.8622998250855));
#9008=CARTESIAN_POINT('Ctrl Pts',(-5.12888744491114,12.4171743591843,13.5810498250855));
#9009=CARTESIAN_POINT('Ctrl Pts',(-4.06819264464732,12.0954147460485,13.2997998250855));
#9010=CARTESIAN_POINT('Ctrl Pts',(-3.74643790785961,11.0347256140874,13.0185498250855));
#9011=CARTESIAN_POINT('Ctrl Pts',(-4.44961008867104,10.1779057780296,12.7372998250855));
#9012=CARTESIAN_POINT('Ctrl Pts',(-5.55269199185788,10.2865501028716,12.4560498250855));
#9013=CARTESIAN_POINT('Ctrl Pts',(-6.07519648156484,11.2640879581285,12.1747998250855));
#9014=CARTESIAN_POINT('Ctrl Pts',(-5.55269199185788,12.2416258133854,11.8935498250855));
#9015=CARTESIAN_POINT('Ctrl Pts',(-4.44961008867105,12.3502701382274,11.6122998250855));
#9016=CARTESIAN_POINT('Ctrl Pts',(-3.74643790785961,11.4934503021696,11.3310498250855));
#9017=CARTESIAN_POINT('Ctrl Pts',(-4.06819264464732,10.4327611702086,11.0497998250855));
#9018=CARTESIAN_POINT('Ctrl Pts',(-5.12888744491114,10.1110015570726,10.7685498250855));
#9019=CARTESIAN_POINT('Ctrl Pts',(-5.98569808817465,10.8141801730346,10.4872998250855));
#9020=CARTESIAN_POINT('Ctrl Pts',(-5.87707091221916,11.9172509800544,10.2060498250855));
#9021=CARTESIAN_POINT('Ctrl Pts',(-4.89949968495297,12.4397765761176,9.92479982508546));
#9022=CARTESIAN_POINT('Ctrl Pts',(-3.92202751272141,11.9172307949619,9.64354982508548));
#9023=CARTESIAN_POINT('Ctrl Pts',(-3.81325352813639,10.8142302749319,9.36229982508546));
#9024=CARTESIAN_POINT('Ctrl Pts',(-4.67032952591772,10.1108973734578,9.08104982508548));
#9025=CARTESIAN_POINT('Ctrl Pts',(-5.73051227207974,10.4329698028178,8.79979982508546));
#9026=CARTESIAN_POINT('Ctrl Pts',(-6.05327536604636,11.4930349515209,8.51854982508547));
#9027=CARTESIAN_POINT('Ctrl Pts',(-5.34808002652064,12.3511120738669,8.23729982508547));
#9028=CARTESIAN_POINT('Ctrl Pts',(-4.43251939644262,12.2582555737237,8.00292482508547));
#9029=CARTESIAN_POINT('Ctrl Pts',(-3.98205572967307,11.7536259611005,7.81542482508547));
#9030=CARTESIAN_POINT('Ctrl Pts',(-3.89952178519528,11.4275925196578,7.72167482508547));
#9031=CARTESIAN_POINT('Ctrl Pts',(-3.89952178519528,11.2640879581285,7.67479982508547));
#9032=CARTESIAN_POINT('Ctrl Pts',(-3.89952178519528,11.2640879581285,16.6));
#9033=CARTESIAN_POINT('Ctrl Pts',(-3.89952178519528,11.100463340754,16.553125));
#9034=CARTESIAN_POINT('Ctrl Pts',(-3.98202611573229,10.7745871843551,16.459375));
#9035=CARTESIAN_POINT('Ctrl Pts',(-4.43258063114212,10.2697743643378,16.271875));
#9036=CARTESIAN_POINT('Ctrl Pts',(-5.34805346405984,10.1770907055197,16.0375));
#9037=CARTESIAN_POINT('Ctrl Pts',(-6.05333301021299,11.0351030238058,15.75625));
#9038=CARTESIAN_POINT('Ctrl Pts',(-5.7305291347766,12.0952484733215,15.475));
#9039=CARTESIAN_POINT('Ctrl Pts',(-4.67032720528385,12.41730825404,15.19375));
#9040=CARTESIAN_POINT('Ctrl Pts',(-3.81321563500956,11.71396418737,14.9125));
#9041=CARTESIAN_POINT('Ctrl Pts',(-3.92199706138937,10.6109219094395,14.63125));
#9042=CARTESIAN_POINT('Ctrl Pts',(-4.89949901982681,10.0883621413897,14.35));
#9043=CARTESIAN_POINT('Ctrl Pts',(-5.87710301444863,10.6109032023111,14.06875));
#9044=CARTESIAN_POINT('Ctrl Pts',(-5.98573321383868,11.7140106207574,13.7875));
#9045=CARTESIAN_POINT('Ctrl Pts',(-5.12889498447605,12.4172116991036,13.50625));
#9046=CARTESIAN_POINT('Ctrl Pts',(-4.06816558640322,12.095441826144,13.225));
#9047=CARTESIAN_POINT('Ctrl Pts',(-3.74640046021744,11.0347181280085,12.94375));
#9048=CARTESIAN_POINT('Ctrl Pts',(-4.44959545666081,10.177870497758,12.6625));
#9049=CARTESIAN_POINT('Ctrl Pts',(-5.55271322406204,10.2865183309037,12.38125));
#9050=CARTESIAN_POINT('Ctrl Pts',(-6.07523468001534,11.2640879581285,12.1));
#9051=CARTESIAN_POINT('Ctrl Pts',(-5.55271322406204,12.2416575853533,11.81875));
#9052=CARTESIAN_POINT('Ctrl Pts',(-4.44959545666081,12.3503054184991,11.5375));
#9053=CARTESIAN_POINT('Ctrl Pts',(-3.74640046021743,11.4934577882485,11.25625));
#9054=CARTESIAN_POINT('Ctrl Pts',(-4.06816558640323,10.432734090113,10.975));
#9055=CARTESIAN_POINT('Ctrl Pts',(-5.12889498447604,10.1109642171534,10.69375));
#9056=CARTESIAN_POINT('Ctrl Pts',(-5.98573321383869,10.8141652954996,10.4125));
#9057=CARTESIAN_POINT('Ctrl Pts',(-5.87710301444862,11.9172727139459,10.13125));
#9058=CARTESIAN_POINT('Ctrl Pts',(-4.89949901982682,12.4398137748673,9.85));
#9059=CARTESIAN_POINT('Ctrl Pts',(-3.92199706138938,11.9172540068175,9.56875));
#9060=CARTESIAN_POINT('Ctrl Pts',(-3.81321563500956,10.8142117288869,9.2875));
#9061=CARTESIAN_POINT('Ctrl Pts',(-4.67032720528385,10.110867662217,9.00625));
#9062=CARTESIAN_POINT('Ctrl Pts',(-5.73052913477659,10.4329274429355,8.725));
#9063=CARTESIAN_POINT('Ctrl Pts',(-6.05333301021299,11.4930728924512,8.44374999999999));
#9064=CARTESIAN_POINT('Ctrl Pts',(-5.34805346405984,12.3510852107373,8.16250000000001));
#9065=CARTESIAN_POINT('Ctrl Pts',(-4.43258063114213,12.2584015519192,7.92812499999999));
#9066=CARTESIAN_POINT('Ctrl Pts',(-3.98202611573229,11.7535887319019,7.740625));
#9067=CARTESIAN_POINT('Ctrl Pts',(-3.89952178519528,11.427712575503,7.646875));
#9068=CARTESIAN_POINT('Ctrl Pts',(-3.89952178519528,11.2640879581285,7.6));
#9069=CARTESIAN_POINT('',(-3.89952178519528,11.2640879581285,7.6));
#9070=CARTESIAN_POINT('Ctrl Pts',(-3.89952178519528,11.2640879581285,16.6));
#9071=CARTESIAN_POINT('Ctrl Pts',(-3.89952178519528,11.100463340754,16.553125));
#9072=CARTESIAN_POINT('Ctrl Pts',(-3.98202611573229,10.7745871843551,16.459375));
#9073=CARTESIAN_POINT('Ctrl Pts',(-4.43258063114212,10.2697743643378,16.271875));
#9074=CARTESIAN_POINT('Ctrl Pts',(-5.34805346405984,10.1770907055197,16.0375));
#9075=CARTESIAN_POINT('Ctrl Pts',(-6.05333301021299,11.0351030238058,15.75625));
#9076=CARTESIAN_POINT('Ctrl Pts',(-5.7305291347766,12.0952484733215,15.475));
#9077=CARTESIAN_POINT('Ctrl Pts',(-4.67032720528385,12.41730825404,15.19375));
#9078=CARTESIAN_POINT('Ctrl Pts',(-3.81321563500956,11.71396418737,14.9125));
#9079=CARTESIAN_POINT('Ctrl Pts',(-3.92199706138937,10.6109219094395,14.63125));
#9080=CARTESIAN_POINT('Ctrl Pts',(-4.89949901982681,10.0883621413897,14.35));
#9081=CARTESIAN_POINT('Ctrl Pts',(-5.87710301444863,10.6109032023111,14.06875));
#9082=CARTESIAN_POINT('Ctrl Pts',(-5.98573321383868,11.7140106207574,13.7875));
#9083=CARTESIAN_POINT('Ctrl Pts',(-5.12889498447605,12.4172116991036,13.50625));
#9084=CARTESIAN_POINT('Ctrl Pts',(-4.06816558640322,12.095441826144,13.225));
#9085=CARTESIAN_POINT('Ctrl Pts',(-3.74640046021744,11.0347181280085,12.94375));
#9086=CARTESIAN_POINT('Ctrl Pts',(-4.44959545666081,10.177870497758,12.6625));
#9087=CARTESIAN_POINT('Ctrl Pts',(-5.55271322406204,10.2865183309037,12.38125));
#9088=CARTESIAN_POINT('Ctrl Pts',(-6.07523468001534,11.2640879581285,12.1));
#9089=CARTESIAN_POINT('Ctrl Pts',(-5.55271322406204,12.2416575853533,11.81875));
#9090=CARTESIAN_POINT('Ctrl Pts',(-4.44959545666081,12.3503054184991,11.5375));
#9091=CARTESIAN_POINT('Ctrl Pts',(-3.74640046021743,11.4934577882485,11.25625));
#9092=CARTESIAN_POINT('Ctrl Pts',(-4.06816558640323,10.432734090113,10.975));
#9093=CARTESIAN_POINT('Ctrl Pts',(-5.12889498447604,10.1109642171534,10.69375));
#9094=CARTESIAN_POINT('Ctrl Pts',(-5.98573321383869,10.8141652954996,10.4125));
#9095=CARTESIAN_POINT('Ctrl Pts',(-5.87710301444862,11.9172727139459,10.13125));
#9096=CARTESIAN_POINT('Ctrl Pts',(-4.89949901982682,12.4398137748673,9.85));
#9097=CARTESIAN_POINT('Ctrl Pts',(-3.92199706138938,11.9172540068175,9.56875));
#9098=CARTESIAN_POINT('Ctrl Pts',(-3.81321563500956,10.8142117288869,9.2875));
#9099=CARTESIAN_POINT('Ctrl Pts',(-4.67032720528385,10.110867662217,9.00625));
#9100=CARTESIAN_POINT('Ctrl Pts',(-5.73052913477659,10.4329274429355,8.725));
#9101=CARTESIAN_POINT('Ctrl Pts',(-6.05333301021299,11.4930728924512,8.44374999999999));
#9102=CARTESIAN_POINT('Ctrl Pts',(-5.34805346405984,12.3510852107373,8.16250000000001));
#9103=CARTESIAN_POINT('Ctrl Pts',(-4.43258063114213,12.2584015519192,7.92812499999999));
#9104=CARTESIAN_POINT('Ctrl Pts',(-3.98202611573229,11.7535887319019,7.740625));
#9105=CARTESIAN_POINT('Ctrl Pts',(-3.89952178519528,11.427712575503,7.646875));
#9106=CARTESIAN_POINT('Ctrl Pts',(-3.89952178519528,11.2640879581285,7.6));
#9107=CARTESIAN_POINT('Origin',(-3.64952178519528,11.2640879581285,7.6));
#9108=CARTESIAN_POINT('Origin',(-3.64952178519528,11.2640879581285,7.6));
#11359=UNCERTAINTY_MEASURE_WITH_UNIT(LENGTH_MEASURE(0.01),#11386,
'DISTANCE_ACCURACY_VALUE',
'Maximum model space distance between geometric entities at asserted c
onnectivities');
#11370=UNCERTAINTY_MEASURE_WITH_UNIT(LENGTH_MEASURE(0.01),#11386,
'DISTANCE_ACCURACY_VALUE',
'Maximum model space distance between geometric entities at asserted c
onnectivities');
#11374=(
GEOMETRIC_REPRESENTATION_CONTEXT(3)
GLOBAL_UNCERTAINTY_ASSIGNED_CONTEXT((#11359))
GLOBAL_UNIT_ASSIGNED_CONTEXT((#11386,#11388,#11389))
REPRESENTATION_CONTEXT('','3D')
);
#11385=(
GEOMETRIC_REPRESENTATION_CONTEXT(3)
GLOBAL_UNCERTAINTY_ASSIGNED_CONTEXT((#11370))
GLOBAL_UNIT_ASSIGNED_CONTEXT((#11386,#11388,#11389))
REPRESENTATION_CONTEXT('','3D')
);
#11386=(
LENGTH_UNIT()
NAMED_UNIT(*)
SI_UNIT(.MILLI.,.METRE.)
);
#11388=(
NAMED_UNIT(*)
PLANE_ANGLE_UNIT()
SI_UNIT($,.RADIAN.)
);
#11389=(
NAMED_UNIT(*)
SI_UNIT($,.STERADIAN.)
SOLID_ANGLE_UNIT()
);
#11393=SHAPE_DEFINITION_REPRESENTATION(#11407,#11434);
#11407=PRODUCT_DEFINITION_SHAPE('',$,#11449);
#11434=SHAPE_REPRESENTATION('',(#5789),#11374);
#11445=PRODUCT_DEFINITION_CONTEXT('part definition',#11489,'design');
#11449=PRODUCT_DEFINITION('Spring_01','Spring_01',#11463,#11445);
#11463=PRODUCT_DEFINITION_FORMATION('',$,#11494);
#11489=APPLICATION_CONTEXT(
'Core Data for Automotive Mechanical Design Process');
#11490=PRODUCT_CONTEXT('part definition',#11489,'mechanical');
#11494=PRODUCT('Spring_01','Spring_01',$,(#11490));
#11561=COLOUR_RGB('Grey',0.48,0.52,0.57);
#11562=FILL_AREA_STYLE_COLOUR('',#11561);
#11563=FILL_AREA_STYLE('',(#11562));
#11564=SURFACE_STYLE_FILL_AREA(#11563);
#11565=SURFACE_SIDE_STYLE('',(#11564));
#11566=SURFACE_STYLE_USAGE(.BOTH.,#11565);
#11567=PRESENTATION_STYLE_ASSIGNMENT((#11566));
ENDSEC;
END-ISO-10303-21;
